ISO-10303-21;
HEADER;
FILE_DESCRIPTION (('STEP AP214'),
    '1' );
FILE_NAME ('circlip for shafts normal_din_Circlip DIN 471 - 10 x 1.step',
    '2026-10-25T07:12:54',
    ( '' ),
    ( '' ),
    'SwSTEP 2.0',
    'SolidWorks 2026',
    '' );
FILE_SCHEMA (( 'AUTOMOTIVE_DESIGN' ));
ENDSEC;

DATA;
#37=DIRECTION ( 'NONE',  ( 1.000000000000000000, 0.000000000000000000, 0.000000000000000000 ) ) ;
#51=ORIENTED_EDGE ( 'NONE', *, *, #11790, .T. ) ;
#93=CARTESIAN_POINT ( 'NONE',  ( 2.000000000000000000, -6.429618962271402616, -1.000000000000000000 ) ) ;
#114=CARTESIAN_POINT ( 'NONE',  ( -0.2500000000000000000, -8.096141056083446585, -1.000000000000000000 ) ) ;
#127=DIRECTION ( 'NONE',  ( 0.000000000000000000, 0.000000000000000000, 1.000000000000000000 ) ) ;
#194=EDGE_CURVE ( 'NONE', #11144, #6641, #2280, .T. ) ;
#215=DIRECTION ( 'NONE',  ( 0.000000000000000000, 0.000000000000000000, 1.000000000000000000 ) ) ;
#225=CARTESIAN_POINT ( 'NONE',  ( -0.1481481481481481122, -4.797713218419819903, -1.000000000000000000 ) ) ;
#280=ORIENTED_EDGE ( 'NONE', *, *, #5001, .F. ) ;
#320=FACE_BOUND ( 'NONE', #11284, .T. ) ;
#328=CIRCLE ( 'NONE', #10491, 0.7500000000000000000 ) ;
#362=DIRECTION ( 'NONE',  ( 0.000000000000000000, 0.000000000000000000, 1.000000000000000000 ) ) ;
#379=LINE ( 'NONE', #9030, #7198 ) ;
#396=CARTESIAN_POINT ( 'NONE',  ( 0.000000000000000000, 0.000000000000000000, -1.000000000000000000 ) ) ;
#410=CARTESIAN_POINT ( 'NONE',  ( -3.098410542199071749, -7.060458129626440815, -1.000000000000000000 ) ) ;
#417=EDGE_CURVE ( 'NONE', #8657, #10456, #8533, .T. ) ;
#426=EDGE_CURVE ( 'NONE', #3623, #2660, #6766, .T. ) ;
#430=AXIS2_PLACEMENT_3D ( 'NONE', #5828, #10990, #3471 ) ;
#431=AXIS2_PLACEMENT_3D ( 'NONE', #2374, #4459, #11719 ) ;
#456=EDGE_LOOP ( 'NONE', ( #11196, #2752, #9623, #6234 ) ) ;
#458=DIRECTION ( 'NONE',  ( -0.000000000000000000, -0.000000000000000000, -1.000000000000000000 ) ) ;
#461=VECTOR ( 'NONE', #11830, 1000.000000000000000 ) ;
#477=DIRECTION ( 'NONE',  ( 0.000000000000000000, 0.000000000000000000, 1.000000000000000000 ) ) ;
#513=AXIS2_PLACEMENT_3D ( 'NONE', #5640, #5842, #553 ) ;
#522=DIRECTION ( 'NONE',  ( 1.000000000000000000, 0.000000000000000000, 0.000000000000000000 ) ) ;
#539=ORIENTED_EDGE ( 'NONE', *, *, #10740, .F. ) ;
#553=DIRECTION ( 'NONE',  ( 1.000000000000000000, 0.000000000000000000, 0.000000000000000000 ) ) ;
#558=VECTOR ( 'NONE', #2702, 1000.000000000000000 ) ;
#567=ORIENTED_EDGE ( 'NONE', *, *, #10818, .T. ) ;
#615=DIRECTION ( 'NONE',  ( 1.000000000000000000, 0.000000000000000000, 0.000000000000000000 ) ) ;
#617=AXIS2_PLACEMENT_3D ( 'NONE', #5271, #4088, #8312 ) ;
#630=CIRCLE ( 'NONE', #7973, 0.7500000000000000000 ) ;
#635=CYLINDRICAL_SURFACE ( 'NONE', #9025, 4.799999999999999822 ) ;
#642=FACE_OUTER_BOUND ( 'NONE', #2942, .T. ) ;
#644=DIRECTION ( 'NONE',  ( 1.000000000000000000, 0.000000000000000000, 0.000000000000000000 ) ) ;
#660=DIRECTION ( 'NONE',  ( 1.000000000000000000, 0.000000000000000000, 0.000000000000000000 ) ) ;
#662=EDGE_CURVE ( 'NONE', #1171, #9857, #2301, .T. ) ;
#747=CARTESIAN_POINT ( 'NONE',  ( 0.000000000000000000, 0.000000000000000000, -1.000000000000000000 ) ) ;
#752=ADVANCED_FACE ( 'NONE', ( #10939 ), #13007, .T. ) ;
#759=AXIS2_PLACEMENT_3D ( 'NONE', #12342, #851, #4126 ) ;
#765=DIRECTION ( 'NONE',  ( 0.000000000000000000, 0.000000000000000000, 1.000000000000000000 ) ) ;
#780=EDGE_LOOP ( 'NONE', ( #3669, #13364, #13258, #3786 ) ) ;
#788=LINE ( 'NONE', #7448, #8616 ) ;
#810=ADVANCED_FACE ( 'NONE', ( #3686 ), #6868, .T. ) ;
#814=CARTESIAN_POINT ( 'NONE',  ( 0.000000000000000000, 0.000000000000000000, 0.000000000000000000 ) ) ;
#851=DIRECTION ( 'NONE',  ( 0.000000000000000000, 0.000000000000000000, 1.000000000000000000 ) ) ;
#855=( GEOMETRIC_REPRESENTATION_CONTEXT ( 3 ) GLOBAL_UNCERTAINTY_ASSIGNED_CONTEXT ( ( #10887 ) ) GLOBAL_UNIT_ASSIGNED_CONTEXT ( ( #4614, #12009, #13098 ) ) REPRESENTATION_CONTEXT ( 'NONE', 'WORKASPACE' ) );
#862=ORIENTED_EDGE ( 'NONE', *, *, #1519, .T. ) ;
#878=PLANE ( 'NONE',  #11324 ) ;
#907=AXIS2_PLACEMENT_3D ( 'NONE', #3681, #5697, #9899 ) ;
#918=ADVANCED_FACE ( 'NONE', ( #1809 ), #9970, .T. ) ;
#943=DIRECTION ( 'NONE',  ( -0.000000000000000000, -0.000000000000000000, -1.000000000000000000 ) ) ;
#1003=ORIENTED_EDGE ( 'NONE', *, *, #12384, .T. ) ;
#1030=DIRECTION ( 'NONE',  ( 0.000000000000000000, 0.000000000000000000, 1.000000000000000000 ) ) ;
#1044=CARTESIAN_POINT ( 'NONE',  ( 0.2499999999999966416, -8.096141056083448362, -1.000000000000000000 ) ) ;
#1065=VERTEX_POINT ( 'NONE', #8795 ) ;
#1066=CIRCLE ( 'NONE', #4398, 6.080745460913608902 ) ;
#1067=ORIENTED_EDGE ( 'NONE', *, *, #10529, .F. ) ;
#1069=LINE ( 'NONE', #12828, #12242 ) ;
#1086=DIRECTION ( 'NONE',  ( 1.000000000000000000, 0.000000000000000000, 0.000000000000000000 ) ) ;
#1098=ORIENTED_EDGE ( 'NONE', *, *, #5605, .T. ) ;
#1124=FACE_OUTER_BOUND ( 'NONE', #456, .T. ) ;
#1131=ADVANCED_FACE ( 'NONE', ( #1446, #2354, #4579 ), #1377, .F. ) ;
#1146=DIRECTION ( 'NONE',  ( 1.000000000000000000, 0.000000000000000000, 0.000000000000000000 ) ) ;
#1151=DIRECTION ( 'NONE',  ( 0.000000000000000000, 0.000000000000000000, 1.000000000000000000 ) ) ;
#1161=DIRECTION ( 'NONE',  ( 0.000000000000000000, 0.000000000000000000, 1.000000000000000000 ) ) ;
#1163=DIRECTION ( 'NONE',  ( 1.000000000000000000, 0.000000000000000000, 0.000000000000000000 ) ) ;
#1171=VERTEX_POINT ( 'NONE', #8736 ) ;
#1193=VECTOR ( 'NONE', #7398, 1000.000000000000000 ) ;
#1207=CARTESIAN_POINT ( 'NONE',  ( 2.354826896168714434, -6.962563485461402024, -1.000000000000000000 ) ) ;
#1254=AXIS2_PLACEMENT_3D ( 'NONE', #12307, #7961, #7061 ) ;
#1270=DIRECTION ( 'NONE',  ( 0.000000000000000000, 0.000000000000000000, 1.000000000000000000 ) ) ;
#1300=EDGE_CURVE ( 'NONE', #1171, #6264, #7965, .T. ) ;
#1319=DIRECTION ( 'NONE',  ( 0.03086419753086420623, -0.9995235871707959241, 0.000000000000000000 ) ) ;
#1330=CARTESIAN_POINT ( 'NONE',  ( -2.595115354961444076, -7.673029147243174641, -1.000000000000000000 ) ) ;
#1377=PLANE ( 'NONE',  #6559 ) ;
#1405=CIRCLE ( 'NONE', #10911, 4.799999999999999822 ) ;
#1406=VERTEX_POINT ( 'NONE', #9475 ) ;
#1414=CIRCLE ( 'NONE', #10486, 4.799999999999999822 ) ;
#1446=FACE_BOUND ( 'NONE', #1985, .T. ) ;
#1453=AXIS2_PLACEMENT_3D ( 'NONE', #814, #10307, #1086 ) ;
#1464=EDGE_CURVE ( 'NONE', #11796, #9525, #9423, .T. ) ;
#1481=DIRECTION ( 'NONE',  ( -0.000000000000000000, -0.000000000000000000, -1.000000000000000000 ) ) ;
#1507=ORIENTED_EDGE ( 'NONE', *, *, #5001, .T. ) ;
#1519=EDGE_CURVE ( 'NONE', #9950, #8373, #6946, .T. ) ;
#1526=AXIS2_PLACEMENT_3D ( 'NONE', #3445, #1481, #13036 ) ;
#1536=DIRECTION ( 'NONE',  ( 0.1305261922200524616, -0.9914448613738103822, 0.000000000000000000 ) ) ;
#1542=VERTEX_POINT ( 'NONE', #8362 ) ;
#1544=CIRCLE ( 'NONE', #12812, 8.099999999999999645 ) ;
#1557=ORIENTED_EDGE ( 'NONE', *, *, #3321, .F. ) ;
#1558=VERTEX_POINT ( 'NONE', #6097 ) ;
#1560=ORIENTED_EDGE ( 'NONE', *, *, #2352, .F. ) ;
#1576=EDGE_LOOP ( 'NONE', ( #9237, #13205, #11519, #1067, #3030, #7455, #3687, #13521, #13342, #12302, #6157, #9485, #5285, #1577, #6093, #1560 ) ) ;
#1577=ORIENTED_EDGE ( 'NONE', *, *, #662, .F. ) ;
#1578=ORIENTED_EDGE ( 'NONE', *, *, #11357, .T. ) ;
#1675=CARTESIAN_POINT ( 'NONE',  ( 0.1481481481481481122, -4.797713218419819903, 0.000000000000000000 ) ) ;
#1683=FACE_OUTER_BOUND ( 'NONE', #4420, .T. ) ;
#1686=FILL_AREA_STYLE ('',( #6759 ) ) ;
#1691=DIRECTION ( 'NONE',  ( 0.1305261922200524338, 0.9914448613738102711, 0.000000000000000000 ) ) ;
#1711=DIRECTION ( 'NONE',  ( 0.000000000000000000, 0.000000000000000000, 1.000000000000000000 ) ) ;
#1717=VECTOR ( 'NONE', #3029, 1000.000000000000000 ) ;
#1750=AXIS2_PLACEMENT_3D ( 'NONE', #3863, #13247, #7885 ) ;
#1757=LINE ( 'NONE', #11528, #5840 ) ;
#1785=DIRECTION ( 'NONE',  ( 0.03086419753086420623, 0.9995235871707959241, 0.000000000000000000 ) ) ;
#1809=FACE_OUTER_BOUND ( 'NONE', #13519, .T. ) ;
#1814=AXIS2_PLACEMENT_3D ( 'NONE', #4160, #3121, #3952 ) ;
#1824=VERTEX_POINT ( 'NONE', #4409 ) ;
#1836=DIRECTION ( 'NONE',  ( -0.000000000000000000, -0.000000000000000000, -1.000000000000000000 ) ) ;
#1862=AXIS2_PLACEMENT_3D ( 'NONE', #11735, #5396, #4345 ) ;
#1863=EDGE_CURVE ( 'NONE', #3871, #1171, #1405, .T. ) ;
#1872=ADVANCED_FACE ( 'NONE', ( #320, #8767, #8699 ), #10632, .T. ) ;
#1878=VERTEX_POINT ( 'NONE', #5462 ) ;
#1902=EDGE_CURVE ( 'NONE', #3871, #1558, #8498, .T. ) ;
#1903=FACE_OUTER_BOUND ( 'NONE', #3125, .T. ) ;
#1907=CARTESIAN_POINT ( 'NONE',  ( 3.309651814758564736, -5.455921364805393026, 0.000000000000000000 ) ) ;
#1917=ORIENTED_EDGE ( 'NONE', *, *, #7876, .T. ) ;
#1967=DIRECTION ( 'NONE',  ( 0.000000000000000000, 0.000000000000000000, 1.000000000000000000 ) ) ;
#1971=DIRECTION ( 'NONE',  ( 0.000000000000000000, 0.000000000000000000, 1.000000000000000000 ) ) ;
#1973=DIRECTION ( 'NONE',  ( 0.000000000000000000, 0.000000000000000000, 1.000000000000000000 ) ) ;
#1979=LINE ( 'NONE', #13648, #9822 ) ;
#1985=EDGE_LOOP ( 'NONE', ( #12272, #3857 ) ) ;
#1991=EDGE_CURVE ( 'NONE', #12658, #9525, #5931, .T. ) ;
#2022=DIRECTION ( 'NONE',  ( 1.000000000000000000, 0.000000000000000000, 0.000000000000000000 ) ) ;
#2027=AXIS2_PLACEMENT_3D ( 'NONE', #6696, #5868, #10059 ) ;
#2036=DIRECTION ( 'NONE',  ( 1.000000000000000000, 0.000000000000000000, 0.000000000000000000 ) ) ;
#2075=AXIS2_PLACEMENT_3D ( 'NONE', #11915, #13080, #3485 ) ;
#2122=EDGE_CURVE ( 'NONE', #3926, #3999, #2684, .T. ) ;
#2127=CARTESIAN_POINT ( 'NONE',  ( 1.250000000000000000, -6.429618962271402616, -1.000000000000000000 ) ) ;
#2146=EDGE_LOOP ( 'NONE', ( #2804, #4087, #1578, #12361 ) ) ;
#2183=ORIENTED_EDGE ( 'NONE', *, *, #4506, .T. ) ;
#2195=CARTESIAN_POINT ( 'NONE',  ( 0.2499999999999966416, -8.096141056083448362, 0.000000000000000000 ) ) ;
#2224=AXIS2_PLACEMENT_3D ( 'NONE', #5376, #10683, #37 ) ;
#2277=ORIENTED_EDGE ( 'NONE', *, *, #2467, .T. ) ;
#2280=LINE ( 'NONE', #8661, #12207 ) ;
#2301=LINE ( 'NONE', #4320, #4399 ) ;
#2352=EDGE_CURVE ( 'NONE', #4274, #3871, #12836, .T. ) ;
#2354=FACE_BOUND ( 'NONE', #4919, .T. ) ;
#2358=DIRECTION ( 'NONE',  ( 0.000000000000000000, 0.000000000000000000, 1.000000000000000000 ) ) ;
#2365=EDGE_CURVE ( 'NONE', #10456, #10143, #10950, .T. ) ;
#2374=CARTESIAN_POINT ( 'NONE',  ( -1.250000000000000000, -6.429618962271402616, -1.000000000000000000 ) ) ;
#2380=CARTESIAN_POINT ( 'NONE',  ( 3.309651814758564736, -5.455921364805393026, -1.000000000000000000 ) ) ;
#2405=DIRECTION ( 'NONE',  ( 0.000000000000000000, 0.000000000000000000, 1.000000000000000000 ) ) ;
#2414=VERTEX_POINT ( 'NONE', #3763 ) ;
#2434=VERTEX_POINT ( 'NONE', #11156 ) ;
#2435=CARTESIAN_POINT ( 'NONE',  ( 0.000000000000000000, 0.000000000000000000, -1.000000000000000000 ) ) ;
#2467=EDGE_CURVE ( 'NONE', #8373, #1065, #8973, .T. ) ;
#2492=CLOSED_SHELL ( 'NONE', ( #10075, #3181, #810, #918, #7463, #6548, #11141, #3731, #9467, #10389, #12183, #13131, #5361, #8892, #9764, #3910, #752, #9684, #1131, #1872, #8900, #7361 ) ) ;
#2495=CARTESIAN_POINT ( 'NONE',  ( -0.1481481481481481122, -4.797713218419819903, -1.000000000000000000 ) ) ;
#2508=CYLINDRICAL_SURFACE ( 'NONE', #2075, 2.396904916527700102 ) ;
#2537=ORIENTED_EDGE ( 'NONE', *, *, #11577, .F. ) ;
#2558=AXIS2_PLACEMENT_3D ( 'NONE', #11443, #11646, #9376 ) ;
#2575=ORIENTED_EDGE ( 'NONE', *, *, #1863, .T. ) ;
#2654=CARTESIAN_POINT ( 'NONE',  ( 0.000000000000000000, 0.5192545390863916310, -1.000000000000000000 ) ) ;
#2658=VERTEX_POINT ( 'NONE', #3141 ) ;
#2660=VERTEX_POINT ( 'NONE', #11513 ) ;
#2666=SURFACE_SIDE_STYLE ('',( #5658 ) ) ;
#2683=VECTOR ( 'NONE', #8505, 1000.000000000000000 ) ;
#2684=CIRCLE ( 'NONE', #2027, 0.7500000000000000000 ) ;
#2700=DIRECTION ( 'NONE',  ( 0.000000000000000000, 0.000000000000000000, 1.000000000000000000 ) ) ;
#2702=DIRECTION ( 'NONE',  ( 0.000000000000000000, 0.000000000000000000, 1.000000000000000000 ) ) ;
#2713=CARTESIAN_POINT ( 'NONE',  ( 0.000000000000000000, 0.5192545390863916310, -1.000000000000000000 ) ) ;
#2730=CARTESIAN_POINT ( 'NONE',  ( -2.000000000000000000, -6.429618962271402616, -1.000000000000000000 ) ) ;
#2752=ORIENTED_EDGE ( 'NONE', *, *, #8570, .T. ) ;
#2754=CARTESIAN_POINT ( 'NONE',  ( -2.354826896168714434, -6.962563485461402024, -1.000000000000000000 ) ) ;
#2759=CARTESIAN_POINT ( 'NONE',  ( -6.080745460913608902, 0.5192545390863924082, -1.000000000000000000 ) ) ;
#2770=ORIENTED_EDGE ( 'NONE', *, *, #12472, .F. ) ;
#2804=ORIENTED_EDGE ( 'NONE', *, *, #417, .F. ) ;
#2826=CARTESIAN_POINT ( 'NONE',  ( 5.686050877451574337, -5.768780236673276995, -1.000000000000000000 ) ) ;
#2838=AXIS2_PLACEMENT_3D ( 'NONE', #3097, #3859, #8084 ) ;
#2855=( GEOMETRIC_REPRESENTATION_CONTEXT ( 3 ) GLOBAL_UNCERTAINTY_ASSIGNED_CONTEXT ( ( #11500 ) ) GLOBAL_UNIT_ASSIGNED_CONTEXT ( ( #13300, #7865, #6964 ) ) REPRESENTATION_CONTEXT ( 'NONE', 'WORKASPACE' ) );
#2858=CARTESIAN_POINT ( 'NONE',  ( -2.354826896168714434, -6.962563485461402024, 0.000000000000000000 ) ) ;
#2865=ORIENTED_EDGE ( 'NONE', *, *, #2122, .F. ) ;
#2896=EDGE_CURVE ( 'NONE', #3939, #9950, #5494, .T. ) ;
#2922=ORIENTED_EDGE ( 'NONE', *, *, #11155, .F. ) ;
#2930=CARTESIAN_POINT ( 'NONE',  ( -4.799999999999999822, 5.878304635907294211E-16, 0.000000000000000000 ) ) ;
#2942=EDGE_LOOP ( 'NONE', ( #5221, #6786, #12087, #4366 ) ) ;
#2980=ORIENTED_EDGE ( 'NONE', *, *, #6378, .T. ) ;
#2993=EDGE_LOOP ( 'NONE', ( #11127, #3922, #8118, #2980 ) ) ;
#3029=DIRECTION ( 'NONE',  ( 0.000000000000000000, 0.000000000000000000, 1.000000000000000000 ) ) ;
#3030=ORIENTED_EDGE ( 'NONE', *, *, #6297, .F. ) ;
#3065=AXIS2_PLACEMENT_3D ( 'NONE', #12740, #3282, #6479 ) ;
#3097=CARTESIAN_POINT ( 'NONE',  ( -1.250000000000000000, -6.429618962271402616, 0.000000000000000000 ) ) ;
#3121=DIRECTION ( 'NONE',  ( 0.000000000000000000, 0.000000000000000000, 1.000000000000000000 ) ) ;
#3125=EDGE_LOOP ( 'NONE', ( #7895, #2865, #12528, #567 ) ) ;
#3141=CARTESIAN_POINT ( 'NONE',  ( -0.1481481481481481122, -4.797713218419819903, 0.000000000000000000 ) ) ;
#3181=ADVANCED_FACE ( 'NONE', ( #9284 ), #13339, .F. ) ;
#3203=CIRCLE ( 'NONE', #4085, 6.080745460913608902 ) ;
#3216=CARTESIAN_POINT ( 'NONE',  ( -4.799999999999999822, 5.878304635907294211E-16, -1.000000000000000000 ) ) ;
#3236=AXIS2_PLACEMENT_3D ( 'NONE', #6346, #1967, #2036 ) ;
#3282=DIRECTION ( 'NONE',  ( -0.000000000000000000, -0.000000000000000000, -1.000000000000000000 ) ) ;
#3321=EDGE_CURVE ( 'NONE', #3999, #3926, #9342, .T. ) ;
#3367=ORIENTED_EDGE ( 'NONE', *, *, #2365, .T. ) ;
#3379=LINE ( 'NONE', #6373, #6011 ) ;
#3399=EDGE_LOOP ( 'NONE', ( #280, #2770 ) ) ;
#3445=CARTESIAN_POINT ( 'NONE',  ( 0.000000000000000000, 0.000000000000000000, 0.000000000000000000 ) ) ;
#3468=ORIENTED_EDGE ( 'NONE', *, *, #10740, .T. ) ;
#3471=DIRECTION ( 'NONE',  ( 1.000000000000000000, 0.000000000000000000, 0.000000000000000000 ) ) ;
#3473=DIRECTION ( 'NONE',  ( 0.000000000000000000, 0.000000000000000000, 1.000000000000000000 ) ) ;
#3485=DIRECTION ( 'NONE',  ( 1.000000000000000000, 0.000000000000000000, 0.000000000000000000 ) ) ;
#3512=DIRECTION ( 'NONE',  ( -0.9995235871707960351, -0.03086419753086420970, 0.000000000000000000 ) ) ;
#3552=EDGE_LOOP ( 'NONE', ( #12358, #539, #8027, #4846 ) ) ;
#3562=LINE ( 'NONE', #3633, #12990 ) ;
#3613=CARTESIAN_POINT ( 'NONE',  ( 0.000000000000000000, 0.000000000000000000, -1.000000000000000000 ) ) ;
#3621=DIRECTION ( 'NONE',  ( 0.000000000000000000, 0.000000000000000000, 1.000000000000000000 ) ) ;
#3623=VERTEX_POINT ( 'NONE', #8095 ) ;
#3633=CARTESIAN_POINT ( 'NONE',  ( 6.080745460913608902, 0.5192545390863916310, -1.000000000000000000 ) ) ;
#3642=AXIS2_PLACEMENT_3D ( 'NONE', #9189, #13452, #12634 ) ;
#3646=CARTESIAN_POINT ( 'NONE',  ( 2.595115354961440524, -7.673029147243177306, -1.000000000000000000 ) ) ;
#3669=ORIENTED_EDGE ( 'NONE', *, *, #8570, .F. ) ;
#3681=CARTESIAN_POINT ( 'NONE',  ( 0.000000000000000000, 0.5192545390863916310, -1.000000000000000000 ) ) ;
#3686=FACE_OUTER_BOUND ( 'NONE', #9273, .T. ) ;
#3687=ORIENTED_EDGE ( 'NONE', *, *, #6225, .F. ) ;
#3694=CARTESIAN_POINT ( 'NONE',  ( -3.309651814758565180, -5.455921364805393026, 0.000000000000000000 ) ) ;
#3728=CIRCLE ( 'NONE', #11467, 6.080745460913608902 ) ;
#3730=VERTEX_POINT ( 'NONE', #114 ) ;
#3731=ADVANCED_FACE ( 'NONE', ( #8304 ), #878, .T. ) ;
#3763=CARTESIAN_POINT ( 'NONE',  ( 6.080745460913608902, 0.5192545390863916310, -1.000000000000000000 ) ) ;
#3772=DIRECTION ( 'NONE',  ( 0.000000000000000000, 0.000000000000000000, 1.000000000000000000 ) ) ;
#3773=VECTOR ( 'NONE', #9334, 999.9999999999998863 ) ;
#3786=ORIENTED_EDGE ( 'NONE', *, *, #9731, .F. ) ;
#3812=DIRECTION ( 'NONE',  ( 0.000000000000000000, 0.000000000000000000, 1.000000000000000000 ) ) ;
#3833=DIRECTION ( 'NONE',  ( 1.000000000000000000, 0.000000000000000000, 0.000000000000000000 ) ) ;
#3841=DIRECTION ( 'NONE',  ( 1.000000000000000000, 0.000000000000000000, 0.000000000000000000 ) ) ;
#3843=LINE ( 'NONE', #6963, #4003 ) ;
#3857=ORIENTED_EDGE ( 'NONE', *, *, #3321, .T. ) ;
#3859=DIRECTION ( 'NONE',  ( 0.000000000000000000, 0.000000000000000000, 1.000000000000000000 ) ) ;
#3863=CARTESIAN_POINT ( 'NONE',  ( 1.250000000000000000, -6.429618962271402616, -1.000000000000000000 ) ) ;
#3868=DIRECTION ( 'NONE',  ( 0.9995235871707960351, -0.03086419753086420970, 0.000000000000000000 ) ) ;
#3871=VERTEX_POINT ( 'NONE', #7518 ) ;
#3875=ORIENTED_EDGE ( 'NONE', *, *, #6349, .T. ) ;
#3910=ADVANCED_FACE ( 'NONE', ( #10954 ), #7587, .T. ) ;
#3912=CARTESIAN_POINT ( 'NONE',  ( 3.098410542199072637, -7.060458129626440815, -1.000000000000000000 ) ) ;
#3922=ORIENTED_EDGE ( 'NONE', *, *, #1300, .F. ) ;
#3926=VERTEX_POINT ( 'NONE', #5581 ) ;
#3939=VERTEX_POINT ( 'NONE', #2380 ) ;
#3941=CIRCLE ( 'NONE', #10564, 4.799999999999999822 ) ;
#3952=DIRECTION ( 'NONE',  ( 1.000000000000000000, 0.000000000000000000, 0.000000000000000000 ) ) ;
#3999=VERTEX_POINT ( 'NONE', #2730 ) ;
#4003=VECTOR ( 'NONE', #11309, 1000.000000000000114 ) ;
#4012=VECTOR ( 'NONE', #477, 1000.000000000000000 ) ;
#4039=SHAPE_DEFINITION_REPRESENTATION ( #6565, #11930 ) ;
#4055=DIRECTION ( 'NONE',  ( 1.000000000000000000, 0.000000000000000000, 0.000000000000000000 ) ) ;
#4085=AXIS2_PLACEMENT_3D ( 'NONE', #9037, #5802, #9998 ) ;
#4087=ORIENTED_EDGE ( 'NONE', *, *, #5599, .F. ) ;
#4088=DIRECTION ( 'NONE',  ( 0.000000000000000000, 0.000000000000000000, 1.000000000000000000 ) ) ;
#4126=DIRECTION ( 'NONE',  ( 1.000000000000000000, 0.000000000000000000, 0.000000000000000000 ) ) ;
#4130=DIRECTION ( 'NONE',  ( 0.03086419753086420623, -0.9995235871707959241, 0.000000000000000000 ) ) ;
#4160=CARTESIAN_POINT ( 'NONE',  ( 1.250000000000000000, -6.429618962271402616, -1.000000000000000000 ) ) ;
#4207=FACE_OUTER_BOUND ( 'NONE', #9744, .T. ) ;
#4212=FACE_OUTER_BOUND ( 'NONE', #3552, .T. ) ;
#4248=CARTESIAN_POINT ( 'NONE',  ( 3.309651814758565180, -5.455921364805393026, 0.000000000000000000 ) ) ;
#4273=EDGE_LOOP ( 'NONE', ( #8712, #9484, #11522, #5387 ) ) ;
#4274=VERTEX_POINT ( 'NONE', #3216 ) ;
#4276=DIRECTION ( 'NONE',  ( 1.000000000000000000, 0.000000000000000000, 0.000000000000000000 ) ) ;
#4320=CARTESIAN_POINT ( 'NONE',  ( 0.1481481481481481122, -4.797713218419819903, -1.000000000000000000 ) ) ;
#4345=DIRECTION ( 'NONE',  ( 1.000000000000000000, 0.000000000000000000, -0.000000000000000000 ) ) ;
#4348=DIRECTION ( 'NONE',  ( 1.000000000000000000, 0.000000000000000000, 0.000000000000000000 ) ) ;
#4366=ORIENTED_EDGE ( 'NONE', *, *, #2896, .T. ) ;
#4398=AXIS2_PLACEMENT_3D ( 'NONE', #2654, #6878, #12400 ) ;
#4399=VECTOR ( 'NONE', #1319, 1000.000000000000114 ) ;
#4409=CARTESIAN_POINT ( 'NONE',  ( -4.078421086530219064, -3.990950201428956845, -1.000000000000000000 ) ) ;
#4410=EDGE_CURVE ( 'NONE', #2434, #5304, #5368, .T. ) ;
#4420=EDGE_LOOP ( 'NONE', ( #6211, #2575, #8659, #8992 ) ) ;
#4425=AXIS2_PLACEMENT_3D ( 'NONE', #13400, #5897, #10094 ) ;
#4445=CARTESIAN_POINT ( 'NONE',  ( 3.309651814758564736, -5.455921364805393026, -1.000000000000000000 ) ) ;
#4459=DIRECTION ( 'NONE',  ( 0.000000000000000000, 0.000000000000000000, 1.000000000000000000 ) ) ;
#4506=EDGE_CURVE ( 'NONE', #1558, #6264, #1414, .T. ) ;
#4524=DIRECTION ( 'NONE',  ( 0.000000000000000000, 0.000000000000000000, 1.000000000000000000 ) ) ;
#4530=CYLINDRICAL_SURFACE ( 'NONE', #431, 0.7500000000000000000 ) ;
#4542=CARTESIAN_POINT ( 'NONE',  ( 2.354826896168714434, -6.962563485461402024, -1.000000000000000000 ) ) ;
#4557=DIRECTION ( 'NONE',  ( 1.000000000000000000, 0.000000000000000000, 0.000000000000000000 ) ) ;
#4579=FACE_OUTER_BOUND ( 'NONE', #1576, .T. ) ;
#4584=EDGE_CURVE ( 'NONE', #13041, #2414, #3203, .T. ) ;
#4585=CARTESIAN_POINT ( 'NONE',  ( 2.000000000000000000, -6.429618962271402616, 0.000000000000000000 ) ) ;
#4589=DIRECTION ( 'NONE',  ( 1.000000000000000000, 0.000000000000000000, 0.000000000000000000 ) ) ;
#4597=( GEOMETRIC_REPRESENTATION_CONTEXT ( 3 ) GLOBAL_UNCERTAINTY_ASSIGNED_CONTEXT ( ( #13412 ) ) GLOBAL_UNIT_ASSIGNED_CONTEXT ( ( #11899, #5424, #4646 ) ) REPRESENTATION_CONTEXT ( 'NONE', 'WORKASPACE' ) );
#4602=DIRECTION ( 'NONE',  ( 0.000000000000000000, 0.000000000000000000, 1.000000000000000000 ) ) ;
#4610=DIRECTION ( 'NONE',  ( -1.000000000000000000, 0.000000000000000000, 0.000000000000000000 ) ) ;
#4614=( LENGTH_UNIT ( ) NAMED_UNIT ( * ) SI_UNIT ( .MILLI., .METRE. ) );
#4628=COLOUR_RGB ( '',1.000000000000000000, 0.9490196078431372140, 0.9098039215686274384 ) ;
#4646=( NAMED_UNIT ( * ) SI_UNIT ( $, .STERADIAN. ) SOLID_ANGLE_UNIT ( ) );
#4673=CIRCLE ( 'NONE', #9096, 0.7499999999999997780 ) ;
#4682=SURFACE_STYLE_USAGE ( .BOTH. , #2666 ) ;
#4684=EDGE_CURVE ( 'NONE', #7378, #11021, #1979, .T. ) ;
#4702=CYLINDRICAL_SURFACE ( 'NONE', #12782, 2.396904916527699214 ) ;
#4711=ORIENTED_EDGE ( 'NONE', *, *, #1519, .F. ) ;
#4797=ORIENTED_EDGE ( 'NONE', *, *, #1991, .F. ) ;
#4815=CARTESIAN_POINT ( 'NONE',  ( 2.595115354961440524, -7.673029147243177306, -1.000000000000000000 ) ) ;
#4836=FACE_OUTER_BOUND ( 'NONE', #12255, .T. ) ;
#4846=ORIENTED_EDGE ( 'NONE', *, *, #9911, .T. ) ;
#4861=AXIS2_PLACEMENT_3D ( 'NONE', #13280, #3621, #615 ) ;
#4891=DIRECTION ( 'NONE',  ( 0.000000000000000000, 0.000000000000000000, 1.000000000000000000 ) ) ;
#4893=PLANE ( 'NONE',  #11264 ) ;
#4919=EDGE_LOOP ( 'NONE', ( #12437, #7148 ) ) ;
#4926=CYLINDRICAL_SURFACE ( 'NONE', #7117, 4.799999999999999822 ) ;
#4951=CARTESIAN_POINT ( 'NONE',  ( -3.309651814758565180, -5.455921364805393026, -1.000000000000000000 ) ) ;
#4997=CARTESIAN_POINT ( 'NONE',  ( 4.078421086530217288, -3.990950201428958621, 0.000000000000000000 ) ) ;
#4998=CARTESIAN_POINT ( 'NONE',  ( 0.1481481481481481122, -4.797713218419819903, -1.000000000000000000 ) ) ;
#5001=EDGE_CURVE ( 'NONE', #5304, #6641, #5801, .T. ) ;
#5051=CARTESIAN_POINT ( 'NONE',  ( 3.309651814758565180, -5.455921364805393026, -1.000000000000000000 ) ) ;
#5078=ORIENTED_EDGE ( 'NONE', *, *, #1464, .T. ) ;
#5085=DIRECTION ( 'NONE',  ( 0.000000000000000000, 0.000000000000000000, 1.000000000000000000 ) ) ;
#5101=CARTESIAN_POINT ( 'NONE',  ( 0.000000000000000000, 0.000000000000000000, -1.000000000000000000 ) ) ;
#5174=CARTESIAN_POINT ( 'NONE',  ( 0.5000000000000000000, -6.429618962271402616, -1.000000000000000000 ) ) ;
#5221=ORIENTED_EDGE ( 'NONE', *, *, #6349, .F. ) ;
#5233=LINE ( 'NONE', #1044, #5357 ) ;
#5271=CARTESIAN_POINT ( 'NONE',  ( 0.000000000000000000, 0.5192545390863916310, 0.000000000000000000 ) ) ;
#5282=CIRCLE ( 'NONE', #9686, 6.080745460913608902 ) ;
#5284=EDGE_CURVE ( 'NONE', #8238, #2658, #9701, .T. ) ;
#5285=ORIENTED_EDGE ( 'NONE', *, *, #8645, .F. ) ;
#5304=VERTEX_POINT ( 'NONE', #4585 ) ;
#5357=VECTOR ( 'NONE', #10467, 1000.000000000000000 ) ;
#5361=ADVANCED_FACE ( 'NONE', ( #10935 ), #13140, .T. ) ;
#5368=LINE ( 'NONE', #93, #7181 ) ;
#5376=CARTESIAN_POINT ( 'NONE',  ( 0.000000000000000000, 0.000000000000000000, -1.000000000000000000 ) ) ;
#5387=ORIENTED_EDGE ( 'NONE', *, *, #5284, .T. ) ;
#5396=DIRECTION ( 'NONE',  ( 0.000000000000000000, 0.000000000000000000, 1.000000000000000000 ) ) ;
#5401=DIRECTION ( 'NONE',  ( 0.000000000000000000, 0.000000000000000000, 1.000000000000000000 ) ) ;
#5424=( NAMED_UNIT ( * ) PLANE_ANGLE_UNIT ( ) SI_UNIT ( $, .RADIAN. ) );
#5462=CARTESIAN_POINT ( 'NONE',  ( -2.000000000000000000, -6.429618962271402616, 0.000000000000000000 ) ) ;
#5494=LINE ( 'NONE', #4445, #6037 ) ;
#5502=CIRCLE ( 'NONE', #3065, 2.396904916527700102 ) ;
#5566=CARTESIAN_POINT ( 'NONE',  ( 0.000000000000000000, 0.5192545390863916310, 0.000000000000000000 ) ) ;
#5580=VECTOR ( 'NONE', #9165, 999.9999999999998863 ) ;
#5581=CARTESIAN_POINT ( 'NONE',  ( -0.5000000000000000000, -6.429618962271402616, -1.000000000000000000 ) ) ;
#5599=EDGE_CURVE ( 'NONE', #1824, #8657, #9536, .T. ) ;
#5605=EDGE_CURVE ( 'NONE', #13041, #8373, #3379, .T. ) ;
#5640=CARTESIAN_POINT ( 'NONE',  ( -1.250000000000000000, -6.429618962271402616, 0.000000000000000000 ) ) ;
#5658=SURFACE_STYLE_FILL_AREA ( #1686 ) ;
#5683=EDGE_CURVE ( 'NONE', #2414, #8791, #5282, .T. ) ;
#5697=DIRECTION ( 'NONE',  ( 0.000000000000000000, 0.000000000000000000, 1.000000000000000000 ) ) ;
#5796=SHAPE_REPRESENTATION_RELATIONSHIP ( 'NONE' , 'NONE' ,  #11930, #8490 ) ;
#5801=CIRCLE ( 'NONE', #11303, 0.7500000000000000000 ) ;
#5802=DIRECTION ( 'NONE',  ( 0.000000000000000000, 0.000000000000000000, 1.000000000000000000 ) ) ;
#5828=CARTESIAN_POINT ( 'NONE',  ( 0.000000000000000000, 0.000000000000000000, 0.000000000000000000 ) ) ;
#5840=VECTOR ( 'NONE', #1973, 1000.000000000000000 ) ;
#5842=DIRECTION ( 'NONE',  ( 0.000000000000000000, 0.000000000000000000, 1.000000000000000000 ) ) ;
#5868=DIRECTION ( 'NONE',  ( 0.000000000000000000, 0.000000000000000000, 1.000000000000000000 ) ) ;
#5897=DIRECTION ( 'NONE',  ( -0.000000000000000000, -0.000000000000000000, -1.000000000000000000 ) ) ;
#5931=LINE ( 'NONE', #3646, #9541 ) ;
#6005=DIRECTION ( 'NONE',  ( 0.9914448613738102711, -0.1305261922200524338, 0.000000000000000000 ) ) ;
#6011=VECTOR ( 'NONE', #5401, 1000.000000000000000 ) ;
#6034=EDGE_CURVE ( 'NONE', #2414, #1065, #3562, .T. ) ;
#6037=VECTOR ( 'NONE', #8741, 1000.000000000000000 ) ;
#6052=ORIENTED_EDGE ( 'NONE', *, *, #8193, .T. ) ;
#6093=ORIENTED_EDGE ( 'NONE', *, *, #1863, .F. ) ;
#6094=CARTESIAN_POINT ( 'NONE',  ( -2.595115354961444076, -7.673029147243174641, -1.000000000000000000 ) ) ;
#6097=CARTESIAN_POINT ( 'NONE',  ( 4.799999999999999822, 0.000000000000000000, 0.000000000000000000 ) ) ;
#6145=DIRECTION ( 'NONE',  ( 0.000000000000000000, 0.000000000000000000, 1.000000000000000000 ) ) ;
#6155=VERTEX_POINT ( 'NONE', #1330 ) ;
#6157=ORIENTED_EDGE ( 'NONE', *, *, #9007, .F. ) ;
#6211=ORIENTED_EDGE ( 'NONE', *, *, #1902, .F. ) ;
#6225=EDGE_CURVE ( 'NONE', #8791, #1824, #1066, .T. ) ;
#6234=ORIENTED_EDGE ( 'NONE', *, *, #5284, .F. ) ;
#6235=LINE ( 'NONE', #6094, #1717 ) ;
#6242=CARTESIAN_POINT ( 'NONE',  ( 2.595115354961440524, -7.673029147243177306, 0.000000000000000000 ) ) ;
#6251=VECTOR ( 'NONE', #2358, 1000.000000000000000 ) ;
#6264=VERTEX_POINT ( 'NONE', #1675 ) ;
#6278=LINE ( 'NONE', #4248, #8666 ) ;
#6297=EDGE_CURVE ( 'NONE', #1406, #11112, #11227, .T. ) ;
#6308=AXIS2_PLACEMENT_3D ( 'NONE', #11682, #10649, #1163 ) ;
#6345=ORIENTED_EDGE ( 'NONE', *, *, #11577, .T. ) ;
#6346=CARTESIAN_POINT ( 'NONE',  ( 0.000000000000000000, 0.000000000000000000, 0.000000000000000000 ) ) ;
#6349=EDGE_CURVE ( 'NONE', #11021, #9950, #6278, .T. ) ;
#6362=ORIENTED_EDGE ( 'NONE', *, *, #12656, .F. ) ;
#6373=CARTESIAN_POINT ( 'NONE',  ( 4.078421086530217288, -3.990950201428958621, -1.000000000000000000 ) ) ;
#6378=EDGE_CURVE ( 'NONE', #9857, #11796, #5233, .T. ) ;
#6479=DIRECTION ( 'NONE',  ( 1.000000000000000000, 0.000000000000000000, 0.000000000000000000 ) ) ;
#6509=CIRCLE ( 'NONE', #513, 0.7500000000000000000 ) ;
#6514=CARTESIAN_POINT ( 'NONE',  ( -4.078421086530219064, -3.990950201428956845, 0.000000000000000000 ) ) ;
#6548=ADVANCED_FACE ( 'NONE', ( #7963 ), #4926, .F. ) ;
#6559=AXIS2_PLACEMENT_3D ( 'NONE', #3613, #3473, #11831 ) ;
#6565=PRODUCT_DEFINITION_SHAPE ( 'NONE', 'NONE',  #12073 ) ;
#6604=CIRCLE ( 'NONE', #7272, 0.7500000000000000000 ) ;
#6628=EDGE_CURVE ( 'NONE', #3926, #1542, #8172, .T. ) ;
#6630=CARTESIAN_POINT ( 'NONE',  ( 0.000000000000000000, 0.000000000000000000, -1.000000000000000000 ) ) ;
#6641=VERTEX_POINT ( 'NONE', #10509 ) ;
#6696=CARTESIAN_POINT ( 'NONE',  ( -1.250000000000000000, -6.429618962271402616, -1.000000000000000000 ) ) ;
#6701=DIRECTION ( 'NONE',  ( 0.03086419753086420623, -0.9995235871707959241, 0.000000000000000000 ) ) ;
#6747=CARTESIAN_POINT ( 'NONE',  ( 0.000000000000000000, 0.5192545390863916310, 0.000000000000000000 ) ) ;
#6759=FILL_AREA_STYLE_COLOUR ( '', #4628 ) ;
#6766=CIRCLE ( 'NONE', #3236, 8.099999999999999645 ) ;
#6768=ORIENTED_EDGE ( 'NONE', *, *, #12852, .F. ) ;
#6786=ORIENTED_EDGE ( 'NONE', *, *, #4684, .F. ) ;
#6830=AXIS2_PLACEMENT_3D ( 'NONE', #2435, #362, #4589 ) ;
#6868=CYLINDRICAL_SURFACE ( 'NONE', #4861, 6.080745460913608902 ) ;
#6878=DIRECTION ( 'NONE',  ( 0.000000000000000000, 0.000000000000000000, 1.000000000000000000 ) ) ;
#6885=PRODUCT_DEFINITION_CONTEXT ( 'detailed design', #9203, 'design' ) ;
#6888=ORIENTED_EDGE ( 'NONE', *, *, #7727, .F. ) ;
#6909=AXIS2_PLACEMENT_3D ( 'NONE', #9681, #1030, #12848 ) ;
#6923=CARTESIAN_POINT ( 'NONE',  ( -3.309651814758565180, -5.455921364805393026, 0.000000000000000000 ) ) ;
#6937=DIRECTION ( 'NONE',  ( 1.000000000000000000, 0.000000000000000000, 0.000000000000000000 ) ) ;
#6946=CIRCLE ( 'NONE', #6308, 2.396904916527699214 ) ;
#6960=CARTESIAN_POINT ( 'NONE',  ( 1.250000000000000000, -6.429618962271402616, -1.000000000000000000 ) ) ;
#6963=CARTESIAN_POINT ( 'NONE',  ( -0.1481481481481481122, -4.797713218419819903, -1.000000000000000000 ) ) ;
#6964=( NAMED_UNIT ( * ) SI_UNIT ( $, .STERADIAN. ) SOLID_ANGLE_UNIT ( ) );
#6980=CYLINDRICAL_SURFACE ( 'NONE', #1750, 0.7500000000000000000 ) ;
#6984=CARTESIAN_POINT ( 'NONE',  ( 0.000000000000000000, 0.5192545390863916310, -1.000000000000000000 ) ) ;
#6991=ORIENTED_EDGE ( 'NONE', *, *, #10818, .F. ) ;
#6995=FACE_OUTER_BOUND ( 'NONE', #13060, .T. ) ;
#7034=CARTESIAN_POINT ( 'NONE',  ( 0.000000000000000000, 0.000000000000000000, 0.000000000000000000 ) ) ;
#7061=DIRECTION ( 'NONE',  ( 1.000000000000000000, 0.000000000000000000, 0.000000000000000000 ) ) ;
#7097=CARTESIAN_POINT ( 'NONE',  ( -3.098410542199071749, -7.060458129626440815, -1.000000000000000000 ) ) ;
#7112=ORIENTED_EDGE ( 'NONE', *, *, #6628, .F. ) ;
#7117=AXIS2_PLACEMENT_3D ( 'NONE', #747, #3812, #10305 ) ;
#7127=CARTESIAN_POINT ( 'NONE',  ( -0.1481481481481481122, -4.797713218419819903, -1.000000000000000000 ) ) ;
#7131=ORIENTED_EDGE ( 'NONE', *, *, #194, .F. ) ;
#7148=ORIENTED_EDGE ( 'NONE', *, *, #9478, .T. ) ;
#7181=VECTOR ( 'NONE', #8539, 1000.000000000000000 ) ;
#7193=PLANE ( 'NONE',  #3642 ) ;
#7198=VECTOR ( 'NONE', #11098, 1000.000000000000000 ) ;
#7221=ORIENTED_EDGE ( 'NONE', *, *, #6034, .F. ) ;
#7272=AXIS2_PLACEMENT_3D ( 'NONE', #6960, #6145, #10338 ) ;
#7293=ORIENTED_EDGE ( 'NONE', *, *, #4410, .T. ) ;
#7301=AXIS2_PLACEMENT_3D ( 'NONE', #2713, #9904, #6937 ) ;
#7309=AXIS2_PLACEMENT_3D ( 'NONE', #10965, #3512, #6701 ) ;
#7361=ADVANCED_FACE ( 'NONE', ( #1903 ), #11384, .F. ) ;
#7378=VERTEX_POINT ( 'NONE', #3912 ) ;
#7391=EDGE_CURVE ( 'NONE', #3730, #8238, #3843, .T. ) ;
#7398=DIRECTION ( 'NONE',  ( 0.000000000000000000, 0.000000000000000000, 1.000000000000000000 ) ) ;
#7406=AXIS2_PLACEMENT_3D ( 'NONE', #11543, #943, #13523 ) ;
#7442=ORIENTED_EDGE ( 'NONE', *, *, #1464, .F. ) ;
#7448=CARTESIAN_POINT ( 'NONE',  ( -0.2500000000000000000, -8.096141056083446585, -1.000000000000000000 ) ) ;
#7455=ORIENTED_EDGE ( 'NONE', *, *, #11357, .F. ) ;
#7463=ADVANCED_FACE ( 'NONE', ( #1124 ), #12554, .F. ) ;
#7475=LINE ( 'NONE', #10648, #12804 ) ;
#7518=CARTESIAN_POINT ( 'NONE',  ( 4.799999999999999822, 0.000000000000000000, -1.000000000000000000 ) ) ;
#7546=CIRCLE ( 'NONE', #11065, 0.7499999999999997780 ) ;
#7587=CYLINDRICAL_SURFACE ( 'NONE', #9378, 0.7499999999999997780 ) ;
#7655=DIRECTION ( 'NONE',  ( 0.000000000000000000, 0.000000000000000000, 1.000000000000000000 ) ) ;
#7727=EDGE_CURVE ( 'NONE', #9525, #11021, #7546, .T. ) ;
#7776=ORIENTED_EDGE ( 'NONE', *, *, #8130, .T. ) ;
#7789=VECTOR ( 'NONE', #2700, 1000.000000000000000 ) ;
#7861=CARTESIAN_POINT ( 'NONE',  ( 3.098410542199072637, -7.060458129626440815, 0.000000000000000000 ) ) ;
#7865=( NAMED_UNIT ( * ) PLANE_ANGLE_UNIT ( ) SI_UNIT ( $, .RADIAN. ) );
#7874=AXIS2_PLACEMENT_3D ( 'NONE', #6747, #13215, #13289 ) ;
#7876=EDGE_CURVE ( 'NONE', #10143, #3623, #4673, .T. ) ;
#7885=DIRECTION ( 'NONE',  ( 1.000000000000000000, 0.000000000000000000, 0.000000000000000000 ) ) ;
#7895=ORIENTED_EDGE ( 'NONE', *, *, #8130, .F. ) ;
#7943=DIRECTION ( 'NONE',  ( 0.000000000000000000, 0.000000000000000000, 1.000000000000000000 ) ) ;
#7961=DIRECTION ( 'NONE',  ( 0.000000000000000000, 0.000000000000000000, 1.000000000000000000 ) ) ;
#7963=FACE_OUTER_BOUND ( 'NONE', #780, .T. ) ;
#7965=LINE ( 'NONE', #4998, #558 ) ;
#7973=AXIS2_PLACEMENT_3D ( 'NONE', #2127, #127, #4348 ) ;
#8003=CARTESIAN_POINT ( 'NONE',  ( 0.2499999999999966416, -8.096141056083448362, -1.000000000000000000 ) ) ;
#8024=ORIENTED_EDGE ( 'NONE', *, *, #8471, .T. ) ;
#8027=ORIENTED_EDGE ( 'NONE', *, *, #12694, .T. ) ;
#8042=ORIENTED_EDGE ( 'NONE', *, *, #2467, .F. ) ;
#8064=EDGE_LOOP ( 'NONE', ( #7131, #2922, #7293, #1507 ) ) ;
#8084=DIRECTION ( 'NONE',  ( 1.000000000000000000, 0.000000000000000000, 0.000000000000000000 ) ) ;
#8095=CARTESIAN_POINT ( 'NONE',  ( -2.595115354961444076, -7.673029147243174641, 0.000000000000000000 ) ) ;
#8118=ORIENTED_EDGE ( 'NONE', *, *, #662, .T. ) ;
#8130=EDGE_CURVE ( 'NONE', #3999, #1878, #12861, .T. ) ;
#8134=EDGE_LOOP ( 'NONE', ( #6888, #4797, #11195, #9954 ) ) ;
#8165=STYLED_ITEM ( 'NONE', ( #8965 ), #8490 ) ;
#8172=LINE ( 'NONE', #10171, #7789 ) ;
#8191=PRODUCT_CONTEXT ( 'NONE', #9727, 'mechanical' ) ;
#8193=EDGE_CURVE ( 'NONE', #11112, #10143, #10860, .T. ) ;
#8208=DIRECTION ( 'NONE',  ( 0.000000000000000000, 0.000000000000000000, 1.000000000000000000 ) ) ;
#8238=VERTEX_POINT ( 'NONE', #2495 ) ;
#8253=ORIENTED_EDGE ( 'NONE', *, *, #13072, .F. ) ;
#8260=CARTESIAN_POINT ( 'NONE',  ( 2.354826896168714434, -6.962563485461402024, 0.000000000000000000 ) ) ;
#8304=FACE_OUTER_BOUND ( 'NONE', #4273, .T. ) ;
#8312=DIRECTION ( 'NONE',  ( 1.000000000000000000, 0.000000000000000000, 0.000000000000000000 ) ) ;
#8352=CARTESIAN_POINT ( 'NONE',  ( 0.1481481481481481122, -4.797713218419819903, 0.000000000000000000 ) ) ;
#8358=AXIS2_PLACEMENT_3D ( 'NONE', #2754, #7943, #4557 ) ;
#8362=CARTESIAN_POINT ( 'NONE',  ( -0.5000000000000000000, -6.429618962271402616, 0.000000000000000000 ) ) ;
#8363=LINE ( 'NONE', #5051, #3773 ) ;
#8365=CIRCLE ( 'NONE', #2838, 0.7500000000000000000 ) ;
#8373=VERTEX_POINT ( 'NONE', #4997 ) ;
#8454=ORIENTED_EDGE ( 'NONE', *, *, #5599, .T. ) ;
#8471=EDGE_CURVE ( 'NONE', #2658, #13327, #10388, .T. ) ;
#8490=ADVANCED_BREP_SHAPE_REPRESENTATION ( '', ( #10205, #430 ), #2855 ) ;
#8498=LINE ( 'NONE', #9665, #1193 ) ;
#8505=DIRECTION ( 'NONE',  ( 0.000000000000000000, 0.000000000000000000, 1.000000000000000000 ) ) ;
#8523=EDGE_LOOP ( 'NONE', ( #1557, #7776, #9095, #7112 ) ) ;
#8533=CIRCLE ( 'NONE', #2558, 2.396904916527700102 ) ;
#8539=DIRECTION ( 'NONE',  ( 0.000000000000000000, 0.000000000000000000, 1.000000000000000000 ) ) ;
#8570=EDGE_CURVE ( 'NONE', #4274, #13327, #7475, .T. ) ;
#8616=VECTOR ( 'NONE', #11386, 1000.000000000000000 ) ;
#8645=EDGE_CURVE ( 'NONE', #9857, #12658, #1544, .T. ) ;
#8657=VERTEX_POINT ( 'NONE', #6514 ) ;
#8659=ORIENTED_EDGE ( 'NONE', *, *, #1300, .T. ) ;
#8660=ORIENTED_EDGE ( 'NONE', *, *, #10529, .T. ) ;
#8661=CARTESIAN_POINT ( 'NONE',  ( 0.5000000000000000000, -6.429618962271402616, -1.000000000000000000 ) ) ;
#8666=VECTOR ( 'NONE', #10536, 999.9999999999998863 ) ;
#8696=CARTESIAN_POINT ( 'NONE',  ( 1.250000000000000000, -6.429618962271402616, 0.000000000000000000 ) ) ;
#8699=FACE_OUTER_BOUND ( 'NONE', #11659, .T. ) ;
#8712=ORIENTED_EDGE ( 'NONE', *, *, #12384, .F. ) ;
#8736=CARTESIAN_POINT ( 'NONE',  ( 0.1481481481481481122, -4.797713218419819903, -1.000000000000000000 ) ) ;
#8741=DIRECTION ( 'NONE',  ( 0.000000000000000000, 0.000000000000000000, 1.000000000000000000 ) ) ;
#8745=ORIENTED_EDGE ( 'NONE', *, *, #2365, .F. ) ;
#8760=VECTOR ( 'NONE', #1536, 999.9999999999998863 ) ;
#8767=FACE_BOUND ( 'NONE', #3399, .T. ) ;
#8790=MECHANICAL_DESIGN_GEOMETRIC_PRESENTATION_REPRESENTATION('',(#9005),#4597);
#8791=VERTEX_POINT ( 'NONE', #2759 ) ;
#8795=CARTESIAN_POINT ( 'NONE',  ( 6.080745460913608902, 0.5192545390863916310, 0.000000000000000000 ) ) ;
#8810=FACE_OUTER_BOUND ( 'NONE', #2146, .T. ) ;
#8892=ADVANCED_FACE ( 'NONE', ( #4836 ), #4702, .F. ) ;
#8900=ADVANCED_FACE ( 'NONE', ( #12364 ), #6980, .F. ) ;
#8918=ORIENTED_EDGE ( 'NONE', *, *, #9478, .F. ) ;
#8936=CARTESIAN_POINT ( 'NONE',  ( -2.000000000000000000, -6.429618962271402616, -1.000000000000000000 ) ) ;
#8959=ORIENTED_EDGE ( 'NONE', *, *, #6297, .T. ) ;
#8965=PRESENTATION_STYLE_ASSIGNMENT (( #4682 ) ) ;
#8973=CIRCLE ( 'NONE', #7874, 6.080745460913608902 ) ;
#8992=ORIENTED_EDGE ( 'NONE', *, *, #4506, .F. ) ;
#9005=STYLED_ITEM('',(#13705),#10205);
#9007=EDGE_CURVE ( 'NONE', #7378, #3939, #8363, .T. ) ;
#9018=CARTESIAN_POINT ( 'NONE',  ( 1.250000000000000000, -6.429618962271402616, 0.000000000000000000 ) ) ;
#9025=AXIS2_PLACEMENT_3D ( 'NONE', #5101, #1971, #3841 ) ;
#9030=CARTESIAN_POINT ( 'NONE',  ( -3.309651814758565180, -5.455921364805393026, -1.000000000000000000 ) ) ;
#9037=CARTESIAN_POINT ( 'NONE',  ( 0.000000000000000000, 0.5192545390863916310, -1.000000000000000000 ) ) ;
#9095=ORIENTED_EDGE ( 'NONE', *, *, #13072, .T. ) ;
#9096=AXIS2_PLACEMENT_3D ( 'NONE', #2858, #765, #2022 ) ;
#9165=DIRECTION ( 'NONE',  ( 0.1305261922200524616, -0.9914448613738103822, 0.000000000000000000 ) ) ;
#9189=CARTESIAN_POINT ( 'NONE',  ( -3.309651814758565180, -5.455921364805393026, -1.000000000000000000 ) ) ;
#9201=ORIENTED_EDGE ( 'NONE', *, *, #1991, .T. ) ;
#9203=APPLICATION_CONTEXT ( 'automotive_design' ) ;
#9237=ORIENTED_EDGE ( 'NONE', *, *, #10558, .F. ) ;
#9273=EDGE_LOOP ( 'NONE', ( #9810, #9884, #12921, #7221 ) ) ;
#9284=FACE_OUTER_BOUND ( 'NONE', #12974, .T. ) ;
#9305=ORIENTED_EDGE ( 'NONE', *, *, #4410, .F. ) ;
#9334=DIRECTION ( 'NONE',  ( 0.1305261922200524616, 0.9914448613738103822, -0.000000000000000000 ) ) ;
#9342=CIRCLE ( 'NONE', #6909, 0.7500000000000000000 ) ;
#9376=DIRECTION ( 'NONE',  ( 1.000000000000000000, 0.000000000000000000, 0.000000000000000000 ) ) ;
#9378=AXIS2_PLACEMENT_3D ( 'NONE', #1207, #7655, #11860 ) ;
#9423=CIRCLE ( 'NONE', #1453, 8.099999999999999645 ) ;
#9467=ADVANCED_FACE ( 'NONE', ( #4212 ), #10435, .T. ) ;
#9475=CARTESIAN_POINT ( 'NONE',  ( -3.309651814758565180, -5.455921364805393026, -1.000000000000000000 ) ) ;
#9478=EDGE_CURVE ( 'NONE', #11144, #2434, #630, .T. ) ;
#9484=ORIENTED_EDGE ( 'NONE', *, *, #9911, .F. ) ;
#9485=ORIENTED_EDGE ( 'NONE', *, *, #11005, .F. ) ;
#9525=VERTEX_POINT ( 'NONE', #6242 ) ;
#9527=DIRECTION ( 'NONE',  ( 0.03086419753086420623, 0.9995235871707959241, -0.000000000000000000 ) ) ;
#9536=LINE ( 'NONE', #11614, #2683 ) ;
#9541=VECTOR ( 'NONE', #4891, 1000.000000000000000 ) ;
#9623=ORIENTED_EDGE ( 'NONE', *, *, #8471, .F. ) ;
#9665=CARTESIAN_POINT ( 'NONE',  ( 4.799999999999999822, 0.000000000000000000, -1.000000000000000000 ) ) ;
#9676=CIRCLE ( 'NONE', #8358, 0.7499999999999997780 ) ;
#9681=CARTESIAN_POINT ( 'NONE',  ( -1.250000000000000000, -6.429618962271402616, -1.000000000000000000 ) ) ;
#9684=ADVANCED_FACE ( 'NONE', ( #11871 ), #9804, .T. ) ;
#9686=AXIS2_PLACEMENT_3D ( 'NONE', #6984, #1711, #660 ) ;
#9701=LINE ( 'NONE', #225, #6251 ) ;
#9717=FACE_OUTER_BOUND ( 'NONE', #8523, .T. ) ;
#9727=APPLICATION_CONTEXT ( 'automotive_design' ) ;
#9731=EDGE_CURVE ( 'NONE', #13327, #1558, #10809, .T. ) ;
#9734=DIRECTION ( 'NONE',  ( -0.000000000000000000, -0.000000000000000000, -1.000000000000000000 ) ) ;
#9744=EDGE_LOOP ( 'NONE', ( #8745, #6362, #8959, #6052 ) ) ;
#9764=ADVANCED_FACE ( 'NONE', ( #642 ), #4893, .T. ) ;
#9804=PLANE ( 'NONE',  #7309 ) ;
#9810=ORIENTED_EDGE ( 'NONE', *, *, #5683, .T. ) ;
#9822=VECTOR ( 'NONE', #11454, 1000.000000000000000 ) ;
#9857=VERTEX_POINT ( 'NONE', #8003 ) ;
#9884=ORIENTED_EDGE ( 'NONE', *, *, #12852, .T. ) ;
#9895=EDGE_CURVE ( 'NONE', #6264, #11796, #13234, .T. ) ;
#9899=DIRECTION ( 'NONE',  ( 1.000000000000000000, 0.000000000000000000, 0.000000000000000000 ) ) ;
#9904=DIRECTION ( 'NONE',  ( 0.000000000000000000, 0.000000000000000000, 1.000000000000000000 ) ) ;
#9911=EDGE_CURVE ( 'NONE', #3730, #2660, #788, .T. ) ;
#9942=DIRECTION ( 'NONE',  ( 0.000000000000000000, 0.000000000000000000, 1.000000000000000000 ) ) ;
#9950=VERTEX_POINT ( 'NONE', #1907 ) ;
#9954=ORIENTED_EDGE ( 'NONE', *, *, #4684, .T. ) ;
#9970=CYLINDRICAL_SURFACE ( 'NONE', #7301, 6.080745460913608902 ) ;
#9998=DIRECTION ( 'NONE',  ( 1.000000000000000000, 0.000000000000000000, 0.000000000000000000 ) ) ;
#10016=CIRCLE ( 'NONE', #759, 8.099999999999999645 ) ;
#10059=DIRECTION ( 'NONE',  ( 1.000000000000000000, 0.000000000000000000, 0.000000000000000000 ) ) ;
#10075=ADVANCED_FACE ( 'NONE', ( #9717 ), #4530, .F. ) ;
#10094=DIRECTION ( 'NONE',  ( 1.000000000000000000, 0.000000000000000000, 0.000000000000000000 ) ) ;
#10143=VERTEX_POINT ( 'NONE', #12661 ) ;
#10151=DIRECTION ( 'NONE',  ( 1.000000000000000000, 0.000000000000000000, 0.000000000000000000 ) ) ;
#10165=ORIENTED_EDGE ( 'NONE', *, *, #5605, .F. ) ;
#10171=CARTESIAN_POINT ( 'NONE',  ( -0.5000000000000000000, -6.429618962271402616, -1.000000000000000000 ) ) ;
#10181=ORIENTED_EDGE ( 'NONE', *, *, #12273, .T. ) ;
#10192=DIRECTION ( 'NONE',  ( 1.000000000000000000, 0.000000000000000000, 0.000000000000000000 ) ) ;
#10205=MANIFOLD_SOLID_BREP ( 'Body', #2492 ) ;
#10272=CARTESIAN_POINT ( 'NONE',  ( -6.080745460913608902, 0.5192545390863924082, 0.000000000000000000 ) ) ;
#10305=DIRECTION ( 'NONE',  ( 1.000000000000000000, 0.000000000000000000, 0.000000000000000000 ) ) ;
#10307=DIRECTION ( 'NONE',  ( 0.000000000000000000, 0.000000000000000000, 1.000000000000000000 ) ) ;
#10338=DIRECTION ( 'NONE',  ( 1.000000000000000000, 0.000000000000000000, 0.000000000000000000 ) ) ;
#10350=AXIS2_PLACEMENT_3D ( 'NONE', #4542, #3772, #4610 ) ;
#10356=ORIENTED_EDGE ( 'NONE', *, *, #194, .T. ) ;
#10388=CIRCLE ( 'NONE', #4425, 4.799999999999999822 ) ;
#10389=ADVANCED_FACE ( 'NONE', ( #6995 ), #11272, .T. ) ;
#10435=CYLINDRICAL_SURFACE ( 'NONE', #12162, 8.099999999999999645 ) ;
#10456=VERTEX_POINT ( 'NONE', #6923 ) ;
#10467=DIRECTION ( 'NONE',  ( 0.000000000000000000, 0.000000000000000000, 1.000000000000000000 ) ) ;
#10486=AXIS2_PLACEMENT_3D ( 'NONE', #7034, #1836, #644 ) ;
#10491=AXIS2_PLACEMENT_3D ( 'NONE', #8696, #1270, #4276 ) ;
#10509=CARTESIAN_POINT ( 'NONE',  ( 0.5000000000000000000, -6.429618962271402616, 0.000000000000000000 ) ) ;
#10529=EDGE_CURVE ( 'NONE', #11112, #6155, #9676, .T. ) ;
#10536=DIRECTION ( 'NONE',  ( 0.1305261922200524616, 0.9914448613738103822, -0.000000000000000000 ) ) ;
#10558=EDGE_CURVE ( 'NONE', #8238, #4274, #3941, .T. ) ;
#10564=AXIS2_PLACEMENT_3D ( 'NONE', #11111, #458, #522 ) ;
#10583=MECHANICAL_DESIGN_GEOMETRIC_PRESENTATION_REPRESENTATION('',(#8165),#855);
#10632=PLANE ( 'NONE',  #1862 ) ;
#10648=CARTESIAN_POINT ( 'NONE',  ( -4.799999999999999822, 5.878304635907294211E-16, -1.000000000000000000 ) ) ;
#10649=DIRECTION ( 'NONE',  ( -0.000000000000000000, -0.000000000000000000, -1.000000000000000000 ) ) ;
#10683=DIRECTION ( 'NONE',  ( 0.000000000000000000, 0.000000000000000000, 1.000000000000000000 ) ) ;
#10740=EDGE_CURVE ( 'NONE', #6155, #3623, #6235, .T. ) ;
#10809=CIRCLE ( 'NONE', #1526, 4.799999999999999822 ) ;
#10818=EDGE_CURVE ( 'NONE', #1542, #1878, #8365, .T. ) ;
#10860=LINE ( 'NONE', #410, #4012 ) ;
#10886=ORIENTED_EDGE ( 'NONE', *, *, #417, .T. ) ;
#10887=UNCERTAINTY_MEASURE_WITH_UNIT (LENGTH_MEASURE( 1.000000000000000082E-05 ), #4614, 'distance_accuracy_value', 'NONE');
#10911=AXIS2_PLACEMENT_3D ( 'NONE', #6630, #9734, #1146 ) ;
#10935=FACE_OUTER_BOUND ( 'NONE', #11234, .T. ) ;
#10939=FACE_OUTER_BOUND ( 'NONE', #11006, .T. ) ;
#10950=LINE ( 'NONE', #3694, #8760 ) ;
#10954=FACE_OUTER_BOUND ( 'NONE', #8134, .T. ) ;
#10965=CARTESIAN_POINT ( 'NONE',  ( 0.1481481481481481122, -4.797713218419819903, -1.000000000000000000 ) ) ;
#10990=DIRECTION ( 'NONE',  ( 0.000000000000000000, 0.000000000000000000, 1.000000000000000000 ) ) ;
#11005=EDGE_CURVE ( 'NONE', #12658, #7378, #11457, .T. ) ;
#11006=EDGE_LOOP ( 'NONE', ( #7442, #11586, #12547, #9201 ) ) ;
#11021=VERTEX_POINT ( 'NONE', #7861 ) ;
#11065=AXIS2_PLACEMENT_3D ( 'NONE', #8260, #5085, #12463 ) ;
#11098=DIRECTION ( 'NONE',  ( 0.000000000000000000, 0.000000000000000000, 1.000000000000000000 ) ) ;
#11111=CARTESIAN_POINT ( 'NONE',  ( 0.000000000000000000, 0.000000000000000000, -1.000000000000000000 ) ) ;
#11112=VERTEX_POINT ( 'NONE', #7097 ) ;
#11127=ORIENTED_EDGE ( 'NONE', *, *, #9895, .F. ) ;
#11141=ADVANCED_FACE ( 'NONE', ( #1683 ), #635, .F. ) ;
#11144=VERTEX_POINT ( 'NONE', #5174 ) ;
#11155=EDGE_CURVE ( 'NONE', #2434, #11144, #6604, .T. ) ;
#11156=CARTESIAN_POINT ( 'NONE',  ( 2.000000000000000000, -6.429618962271402616, -1.000000000000000000 ) ) ;
#11172=CARTESIAN_POINT ( 'NONE',  ( 3.309651814758565180, -5.455921364805393026, -1.000000000000000000 ) ) ;
#11195=ORIENTED_EDGE ( 'NONE', *, *, #11005, .T. ) ;
#11196=ORIENTED_EDGE ( 'NONE', *, *, #10558, .T. ) ;
#11226=DIRECTION ( 'NONE',  ( -0.000000000000000000, -0.000000000000000000, -1.000000000000000000 ) ) ;
#11227=LINE ( 'NONE', #4951, #5580 ) ;
#11234=EDGE_LOOP ( 'NONE', ( #6768, #12659, #8454, #2537 ) ) ;
#11264=AXIS2_PLACEMENT_3D ( 'NONE', #11172, #6005, #1691 ) ;
#11272=CYLINDRICAL_SURFACE ( 'NONE', #1254, 0.7499999999999997780 ) ;
#11284=EDGE_LOOP ( 'NONE', ( #6991, #8253 ) ) ;
#11303=AXIS2_PLACEMENT_3D ( 'NONE', #9018, #13214, #3833 ) ;
#11309=DIRECTION ( 'NONE',  ( 0.03086419753086420623, 0.9995235871707959241, -0.000000000000000000 ) ) ;
#11324=AXIS2_PLACEMENT_3D ( 'NONE', #7127, #3868, #1785 ) ;
#11357=EDGE_CURVE ( 'NONE', #1824, #1406, #5502, .T. ) ;
#11384=CYLINDRICAL_SURFACE ( 'NONE', #13477, 0.7500000000000000000 ) ;
#11386=DIRECTION ( 'NONE',  ( 0.000000000000000000, 0.000000000000000000, 1.000000000000000000 ) ) ;
#11401=PRODUCT ( 'circlip for shafts normal_din_Circlip DIN 471 - 10 x 1', 'circlip for shafts normal_din_Circlip DIN 471 - 10 x 1', '', ( #8191 ) ) ;
#11420=ORIENTED_EDGE ( 'NONE', *, *, #7876, .F. ) ;
#11443=CARTESIAN_POINT ( 'NONE',  ( -5.686050877451574337, -5.768780236673276995, 0.000000000000000000 ) ) ;
#11454=DIRECTION ( 'NONE',  ( 0.000000000000000000, 0.000000000000000000, 1.000000000000000000 ) ) ;
#11457=CIRCLE ( 'NONE', #10350, 0.7499999999999997780 ) ;
#11467=AXIS2_PLACEMENT_3D ( 'NONE', #5566, #4524, #13465 ) ;
#11472=DIRECTION ( 'NONE',  ( 1.000000000000000000, 0.000000000000000000, 0.000000000000000000 ) ) ;
#11500=UNCERTAINTY_MEASURE_WITH_UNIT (LENGTH_MEASURE( 1.000000000000000082E-05 ), #13300, 'distance_accuracy_value', 'NONE');
#11513=CARTESIAN_POINT ( 'NONE',  ( -0.2500000000000000000, -8.096141056083446585, 0.000000000000000000 ) ) ;
#11519=ORIENTED_EDGE ( 'NONE', *, *, #12694, .F. ) ;
#11522=ORIENTED_EDGE ( 'NONE', *, *, #7391, .T. ) ;
#11528=CARTESIAN_POINT ( 'NONE',  ( -6.080745460913608902, 0.5192545390863924082, -1.000000000000000000 ) ) ;
#11543=CARTESIAN_POINT ( 'NONE',  ( 5.686050877451574337, -5.768780236673276995, -1.000000000000000000 ) ) ;
#11577=EDGE_CURVE ( 'NONE', #12805, #8657, #3728, .T. ) ;
#11586=ORIENTED_EDGE ( 'NONE', *, *, #6378, .F. ) ;
#11612=CARTESIAN_POINT ( 'NONE',  ( 0.000000000000000000, 0.000000000000000000, -1.000000000000000000 ) ) ;
#11614=CARTESIAN_POINT ( 'NONE',  ( -4.078421086530219064, -3.990950201428956845, -1.000000000000000000 ) ) ;
#11646=DIRECTION ( 'NONE',  ( -0.000000000000000000, -0.000000000000000000, -1.000000000000000000 ) ) ;
#11659=EDGE_LOOP ( 'NONE', ( #8024, #12220, #2183, #13395, #5078, #12171, #3875, #862, #2277, #51, #6345, #10886, #3367, #1917, #13129, #1003 ) ) ;
#11682=CARTESIAN_POINT ( 'NONE',  ( 5.686050877451574337, -5.768780236673276995, 0.000000000000000000 ) ) ;
#11719=DIRECTION ( 'NONE',  ( 1.000000000000000000, 0.000000000000000000, 0.000000000000000000 ) ) ;
#11735=CARTESIAN_POINT ( 'NONE',  ( 0.000000000000000000, 0.000000000000000000, 0.000000000000000000 ) ) ;
#11790=EDGE_CURVE ( 'NONE', #1065, #12805, #12569, .T. ) ;
#11796=VERTEX_POINT ( 'NONE', #2195 ) ;
#11830=DIRECTION ( 'NONE',  ( 0.000000000000000000, 0.000000000000000000, 1.000000000000000000 ) ) ;
#11831=DIRECTION ( 'NONE',  ( 1.000000000000000000, 0.000000000000000000, -0.000000000000000000 ) ) ;
#11860=DIRECTION ( 'NONE',  ( 1.000000000000000000, 0.000000000000000000, 0.000000000000000000 ) ) ;
#11871=FACE_OUTER_BOUND ( 'NONE', #2993, .T. ) ;
#11899=( LENGTH_UNIT ( ) NAMED_UNIT ( * ) SI_UNIT ( .MILLI., .METRE. ) );
#11908=ORIENTED_EDGE ( 'NONE', *, *, #8193, .F. ) ;
#11915=CARTESIAN_POINT ( 'NONE',  ( -5.686050877451574337, -5.768780236673276995, -1.000000000000000000 ) ) ;
#11930=SHAPE_REPRESENTATION ( 'circlip for shafts normal_din_Circlip DIN 471 - 10 x 1', ( #430 ), #2855 ) ;
#12009=( NAMED_UNIT ( * ) PLANE_ANGLE_UNIT ( ) SI_UNIT ( $, .RADIAN. ) );
#12073=PRODUCT_DEFINITION ( 'UNKNOWN', '', #12359, #6885 ) ;
#12087=ORIENTED_EDGE ( 'NONE', *, *, #9007, .T. ) ;
#12120=ORIENTED_EDGE ( 'NONE', *, *, #4584, .T. ) ;
#12162=AXIS2_PLACEMENT_3D ( 'NONE', #11612, #1151, #11472 ) ;
#12171=ORIENTED_EDGE ( 'NONE', *, *, #7727, .T. ) ;
#12183=ADVANCED_FACE ( 'NONE', ( #4207 ), #7193, .T. ) ;
#12207=VECTOR ( 'NONE', #215, 1000.000000000000000 ) ;
#12209=CARTESIAN_POINT ( 'NONE',  ( -1.250000000000000000, -6.429618962271402616, -1.000000000000000000 ) ) ;
#12220=ORIENTED_EDGE ( 'NONE', *, *, #9731, .T. ) ;
#12242=VECTOR ( 'NONE', #9527, 1000.000000000000114 ) ;
#12255=EDGE_LOOP ( 'NONE', ( #4711, #13539, #10181, #1098 ) ) ;
#12265=CARTESIAN_POINT ( 'NONE',  ( 0.000000000000000000, 0.000000000000000000, -1.000000000000000000 ) ) ;
#12272=ORIENTED_EDGE ( 'NONE', *, *, #2122, .T. ) ;
#12273=EDGE_CURVE ( 'NONE', #3939, #13041, #13331, .T. ) ;
#12302=ORIENTED_EDGE ( 'NONE', *, *, #12273, .F. ) ;
#12307=CARTESIAN_POINT ( 'NONE',  ( -2.354826896168714434, -6.962563485461402024, -1.000000000000000000 ) ) ;
#12342=CARTESIAN_POINT ( 'NONE',  ( 0.000000000000000000, 0.000000000000000000, -1.000000000000000000 ) ) ;
#12358=ORIENTED_EDGE ( 'NONE', *, *, #426, .F. ) ;
#12359=PRODUCT_DEFINITION_FORMATION_WITH_SPECIFIED_SOURCE ( 'ANY', '', #11401, .NOT_KNOWN. ) ;
#12361=ORIENTED_EDGE ( 'NONE', *, *, #12656, .T. ) ;
#12364=FACE_OUTER_BOUND ( 'NONE', #8064, .T. ) ;
#12384=EDGE_CURVE ( 'NONE', #2660, #2658, #1069, .T. ) ;
#12400=DIRECTION ( 'NONE',  ( 1.000000000000000000, 0.000000000000000000, 0.000000000000000000 ) ) ;
#12437=ORIENTED_EDGE ( 'NONE', *, *, #11155, .T. ) ;
#12453=ORIENTED_EDGE ( 'NONE', *, *, #6034, .T. ) ;
#12463=DIRECTION ( 'NONE',  ( -1.000000000000000000, 0.000000000000000000, 0.000000000000000000 ) ) ;
#12472=EDGE_CURVE ( 'NONE', #6641, #5304, #328, .T. ) ;
#12528=ORIENTED_EDGE ( 'NONE', *, *, #6628, .T. ) ;
#12547=ORIENTED_EDGE ( 'NONE', *, *, #8645, .T. ) ;
#12554=CYLINDRICAL_SURFACE ( 'NONE', #2224, 4.799999999999999822 ) ;
#12569=CIRCLE ( 'NONE', #617, 6.080745460913608902 ) ;
#12634=DIRECTION ( 'NONE',  ( 0.1305261922200524338, -0.9914448613738102711, 0.000000000000000000 ) ) ;
#12656=EDGE_CURVE ( 'NONE', #1406, #10456, #379, .T. ) ;
#12658=VERTEX_POINT ( 'NONE', #4815 ) ;
#12659=ORIENTED_EDGE ( 'NONE', *, *, #6225, .T. ) ;
#12661=CARTESIAN_POINT ( 'NONE',  ( -3.098410542199071749, -7.060458129626440815, 0.000000000000000000 ) ) ;
#12694=EDGE_CURVE ( 'NONE', #6155, #3730, #10016, .T. ) ;
#12740=CARTESIAN_POINT ( 'NONE',  ( -5.686050877451574337, -5.768780236673276995, -1.000000000000000000 ) ) ;
#12782=AXIS2_PLACEMENT_3D ( 'NONE', #2826, #9942, #10151 ) ;
#12804=VECTOR ( 'NONE', #1161, 1000.000000000000000 ) ;
#12805=VERTEX_POINT ( 'NONE', #10272 ) ;
#12812=AXIS2_PLACEMENT_3D ( 'NONE', #396, #2405, #12978 ) ;
#12828=CARTESIAN_POINT ( 'NONE',  ( -0.1481481481481481122, -4.797713218419819903, 0.000000000000000000 ) ) ;
#12836=CIRCLE ( 'NONE', #13274, 4.799999999999999822 ) ;
#12848=DIRECTION ( 'NONE',  ( 1.000000000000000000, 0.000000000000000000, 0.000000000000000000 ) ) ;
#12852=EDGE_CURVE ( 'NONE', #8791, #12805, #1757, .T. ) ;
#12861=LINE ( 'NONE', #8936, #461 ) ;
#12921=ORIENTED_EDGE ( 'NONE', *, *, #11790, .F. ) ;
#12941=CARTESIAN_POINT ( 'NONE',  ( 4.078421086530217288, -3.990950201428958621, -1.000000000000000000 ) ) ;
#12974=EDGE_LOOP ( 'NONE', ( #8918, #10356, #13279, #9305 ) ) ;
#12978=DIRECTION ( 'NONE',  ( 1.000000000000000000, 0.000000000000000000, 0.000000000000000000 ) ) ;
#12990=VECTOR ( 'NONE', #4602, 1000.000000000000000 ) ;
#13007=CYLINDRICAL_SURFACE ( 'NONE', #6830, 8.099999999999999645 ) ;
#13017=VECTOR ( 'NONE', #4130, 1000.000000000000114 ) ;
#13036=DIRECTION ( 'NONE',  ( 1.000000000000000000, 0.000000000000000000, 0.000000000000000000 ) ) ;
#13041=VERTEX_POINT ( 'NONE', #12941 ) ;
#13060=EDGE_LOOP ( 'NONE', ( #11420, #11908, #8660, #3468 ) ) ;
#13072=EDGE_CURVE ( 'NONE', #1878, #1542, #6509, .T. ) ;
#13080=DIRECTION ( 'NONE',  ( 0.000000000000000000, 0.000000000000000000, 1.000000000000000000 ) ) ;
#13098=( NAMED_UNIT ( * ) SI_UNIT ( $, .STERADIAN. ) SOLID_ANGLE_UNIT ( ) );
#13129=ORIENTED_EDGE ( 'NONE', *, *, #426, .T. ) ;
#13131=ADVANCED_FACE ( 'NONE', ( #8810 ), #2508, .F. ) ;
#13140=CYLINDRICAL_SURFACE ( 'NONE', #907, 6.080745460913608902 ) ;
#13205=ORIENTED_EDGE ( 'NONE', *, *, #7391, .F. ) ;
#13214=DIRECTION ( 'NONE',  ( 0.000000000000000000, 0.000000000000000000, 1.000000000000000000 ) ) ;
#13215=DIRECTION ( 'NONE',  ( 0.000000000000000000, 0.000000000000000000, 1.000000000000000000 ) ) ;
#13234=LINE ( 'NONE', #8352, #13017 ) ;
#13247=DIRECTION ( 'NONE',  ( 0.000000000000000000, 0.000000000000000000, 1.000000000000000000 ) ) ;
#13258=ORIENTED_EDGE ( 'NONE', *, *, #1902, .T. ) ;
#13274=AXIS2_PLACEMENT_3D ( 'NONE', #12265, #11226, #10192 ) ;
#13279=ORIENTED_EDGE ( 'NONE', *, *, #12472, .T. ) ;
#13280=CARTESIAN_POINT ( 'NONE',  ( 0.000000000000000000, 0.5192545390863916310, -1.000000000000000000 ) ) ;
#13289=DIRECTION ( 'NONE',  ( 1.000000000000000000, 0.000000000000000000, 0.000000000000000000 ) ) ;
#13300=( LENGTH_UNIT ( ) NAMED_UNIT ( * ) SI_UNIT ( .MILLI., .METRE. ) );
#13327=VERTEX_POINT ( 'NONE', #2930 ) ;
#13331=CIRCLE ( 'NONE', #7406, 2.396904916527699214 ) ;
#13339=CYLINDRICAL_SURFACE ( 'NONE', #1814, 0.7500000000000000000 ) ;
#13342=ORIENTED_EDGE ( 'NONE', *, *, #4584, .F. ) ;
#13364=ORIENTED_EDGE ( 'NONE', *, *, #2352, .T. ) ;
#13395=ORIENTED_EDGE ( 'NONE', *, *, #9895, .T. ) ;
#13400=CARTESIAN_POINT ( 'NONE',  ( 0.000000000000000000, 0.000000000000000000, 0.000000000000000000 ) ) ;
#13412=UNCERTAINTY_MEASURE_WITH_UNIT (LENGTH_MEASURE( 1.000000000000000082E-05 ), #11899, 'distance_accuracy_value', 'NONE');
#13452=DIRECTION ( 'NONE',  ( -0.9914448613738102711, -0.1305261922200524338, 0.000000000000000000 ) ) ;
#13465=DIRECTION ( 'NONE',  ( 1.000000000000000000, 0.000000000000000000, 0.000000000000000000 ) ) ;
#13477=AXIS2_PLACEMENT_3D ( 'NONE', #12209, #8208, #4055 ) ;
#13519=EDGE_LOOP ( 'NONE', ( #12120, #12453, #8042, #10165 ) ) ;
#13521=ORIENTED_EDGE ( 'NONE', *, *, #5683, .F. ) ;
#13523=DIRECTION ( 'NONE',  ( 1.000000000000000000, 0.000000000000000000, 0.000000000000000000 ) ) ;
#13539=ORIENTED_EDGE ( 'NONE', *, *, #2896, .F. ) ;
#13648=CARTESIAN_POINT ( 'NONE',  ( 3.098410542199072637, -7.060458129626440815, -1.000000000000000000 ) ) ;
#13699=COLOUR_RGB('Grey',0.48,0.52,0.57);
#13700=FILL_AREA_STYLE_COLOUR('',#13699);
#13701=FILL_AREA_STYLE('',(#13700));
#13702=SURFACE_STYLE_FILL_AREA(#13701);
#13703=SURFACE_SIDE_STYLE('',(#13702));
#13704=SURFACE_STYLE_USAGE(.BOTH.,#13703);
#13705=PRESENTATION_STYLE_ASSIGNMENT((#13704));
ENDSEC;
END-ISO-10303-21;
